ISO-10303-21;
HEADER;
FILE_DESCRIPTION (('STEP AP214'),
    '1' );
FILE_NAME ('socket head cap screw_iso_ISO 4762 M4 x 16 - 16N.step',
    '2026-10-08T12:12:07',
    ( '' ),
    ( '' ),
    'SwSTEP 2.0',
    'SolidWorks 2026',
    '' );
FILE_SCHEMA (( 'AUTOMOTIVE_DESIGN' ));
ENDSEC;

DATA;
#5=PRODUCT_DEFINITION_SHAPE ( 'NONE', 'NONE',  #2283 ) ;
#26=CARTESIAN_POINT ( 'NONE',  ( 0.1999999999999987899, 0.000000000000000000, 0.000000000000000000 ) ) ;
#53=MECHANICAL_DESIGN_GEOMETRIC_PRESENTATION_REPRESENTATION('',(#5634),#3784);
#66=LINE ( 'NONE', #3278, #5122 ) ;
#87=CARTESIAN_POINT ( 'NONE',  ( 4.000000000000003553, 4.286263797015736595E-16, -3.500000000000000000 ) ) ;
#107=DIRECTION ( 'NONE',  ( -1.000000000000000000, -0.000000000000000000, -0.000000000000000000 ) ) ;
#114=VECTOR ( 'NONE', #3066, 1000.000000000000000 ) ;
#118=VECTOR ( 'NONE', #3051, 1000.000000000000000 ) ;
#140=( NAMED_UNIT ( * ) PLANE_ANGLE_UNIT ( ) SI_UNIT ( $, .RADIAN. ) );
#170=EDGE_LOOP ( 'NONE', ( #610, #780, #5868, #1620, #3543 ) ) ;
#173=CARTESIAN_POINT ( 'NONE',  ( 2.000000000000000000, 1.773042676681340968, -2.276824562219559311E-15 ) ) ;
#181=ADVANCED_FACE ( 'NONE', ( #1112 ), #7964, .F. ) ;
#184=CARTESIAN_POINT ( 'NONE',  ( 0.000000000000000000, -1.773042676681340524, 1.734723475976807094E-15 ) ) ;
#186=DIRECTION ( 'NONE',  ( 0.000000000000000000, 0.000000000000000000, 1.000000000000000000 ) ) ;
#189=VERTEX_POINT ( 'NONE', #8093 ) ;
#199=ORIENTED_EDGE ( 'NONE', *, *, #8204, .F. ) ;
#206=AXIS2_PLACEMENT_3D ( 'NONE', #1783, #7378, #1108 ) ;
#208=DIRECTION ( 'NONE',  ( 0.000000000000000000, 0.000000000000000000, 1.000000000000000000 ) ) ;
#209=DIRECTION ( 'NONE',  ( -1.000000000000000000, -0.000000000000000000, -0.000000000000000000 ) ) ;
#212=DIRECTION ( 'NONE',  ( -1.000000000000000000, -0.000000000000000000, -0.000000000000000000 ) ) ;
#214=ORIENTED_EDGE ( 'NONE', *, *, #5188, .T. ) ;
#216=ADVANCED_FACE ( 'NONE', ( #5490 ), #4856, .T. ) ;
#261=ORIENTED_EDGE ( 'NONE', *, *, #7341, .T. ) ;
#273=ORIENTED_EDGE ( 'NONE', *, *, #5939, .F. ) ;
#277=AXIS2_PLACEMENT_3D ( 'NONE', #6846, #6974, #1289 ) ;
#283=ORIENTED_EDGE ( 'NONE', *, *, #342, .T. ) ;
#311=ORIENTED_EDGE ( 'NONE', *, *, #3355, .T. ) ;
#331=DIRECTION ( 'NONE',  ( -0.7071067811865355823, 0.000000000000000000, 0.7071067811865595631 ) ) ;
#342=EDGE_CURVE ( 'NONE', #1297, #5311, #66, .T. ) ;
#351=ADVANCED_FACE ( 'NONE', ( #5809 ), #6431, .T. ) ;
#352=ORIENTED_EDGE ( 'NONE', *, *, #4978, .F. ) ;
#367=CARTESIAN_POINT ( 'NONE',  ( 2.000000000000000000, 0.000000000000000000, 0.000000000000000000 ) ) ;
#368=AXIS2_PLACEMENT_3D ( 'NONE', #6411, #7765, #5900 ) ;
#378=CIRCLE ( 'NONE', #915, 0.2000000000000000944 ) ;
#388=CIRCLE ( 'NONE', #7708, 3.500000000000000000 ) ;
#389=ORIENTED_EDGE ( 'NONE', *, *, #5878, .F. ) ;
#413=DIRECTION ( 'NONE',  ( -1.000000000000000000, -0.000000000000000000, -0.000000000000000000 ) ) ;
#418=ORIENTED_EDGE ( 'NONE', *, *, #2740, .T. ) ;
#434=EDGE_CURVE ( 'NONE', #4855, #3946, #6691, .T. ) ;
#447=CARTESIAN_POINT ( 'NONE',  ( 0.000000000000000000, -0.8865213383406721492, -1.535499999999998977 ) ) ;
#449=CARTESIAN_POINT ( 'NONE',  ( 4.000000000000003553, 0.000000000000000000, 3.500000000000000000 ) ) ;
#452=VERTEX_POINT ( 'NONE', #6506 ) ;
#462=DIRECTION ( 'NONE',  ( 0.000000000000000000, 0.5000000000000011102, 0.8660254037844379305 ) ) ;
#463=ORIENTED_EDGE ( 'NONE', *, *, #2563, .T. ) ;
#495=AXIS2_PLACEMENT_3D ( 'NONE', #6230, #4451, #4995 ) ;
#501=AXIS2_PLACEMENT_3D ( 'NONE', #1664, #4192, #6723 ) ;
#502=ORIENTED_EDGE ( 'NONE', *, *, #2182, .F. ) ;
#507=ORIENTED_EDGE ( 'NONE', *, *, #4695, .F. ) ;
#508=CONICAL_SURFACE ( 'NONE', #5176, 1.535500000000000087, 1.047197551196590748 ) ;
#511=CIRCLE ( 'NONE', #1453, 1.535500000000000087 ) ;
#522=CARTESIAN_POINT ( 'NONE',  ( -31.74999999999995737, 0.000000000000000000, 0.000000000000000000 ) ) ;
#546=CARTESIAN_POINT ( 'NONE',  ( 4.200000000000001954, 2.449293598294707893E-16, -2.000000000000000888 ) ) ;
#554=VERTEX_POINT ( 'NONE', #4026 ) ;
#566=DIRECTION ( 'NONE',  ( -1.000000000000000000, -0.000000000000000000, -0.000000000000000000 ) ) ;
#568=CARTESIAN_POINT ( 'NONE',  ( 4.000000000000000000, 0.000000000000000000, 0.000000000000000000 ) ) ;
#571=DIRECTION ( 'NONE',  ( 0.000000000000000000, -1.000000000000000000, 1.222984857324291014E-15 ) ) ;
#576=CARTESIAN_POINT ( 'NONE',  ( 0.000000000000000000, 0.000000000000000000, 0.000000000000000000 ) ) ;
#609=LINE ( 'NONE', #3113, #6717 ) ;
#610=ORIENTED_EDGE ( 'NONE', *, *, #4018, .T. ) ;
#623=LINE ( 'NONE', #7572, #7694 ) ;
#643=EDGE_CURVE ( 'NONE', #6632, #2779, #3879, .T. ) ;
#644=CLOSED_SHELL ( 'NONE', ( #6319, #3004, #4176, #1665, #6143, #3927, #6537, #4016, #4322, #2033, #4212, #216, #7611, #5799, #3720, #3409, #351, #4075, #5766, #1524, #4733, #1050, #181, #5566, #5341, #1901, #3631 ) ) ;
#646=AXIS2_PLACEMENT_3D ( 'NONE', #7732, #7883, #5249 ) ;
#665=EDGE_CURVE ( 'NONE', #554, #1216, #623, .T. ) ;
#668=EDGE_LOOP ( 'NONE', ( #7988, #3759, #463, #418 ) ) ;
#676=DIRECTION ( 'NONE',  ( 1.000000000000000000, 0.000000000000000000, 0.000000000000000000 ) ) ;
#727=DIRECTION ( 'NONE',  ( -0.5000000000000061062, 1.060575238724902601E-16, -0.8660254037844351549 ) ) ;
#734=LINE ( 'NONE', #5965, #7798 ) ;
#780=ORIENTED_EDGE ( 'NONE', *, *, #5952, .F. ) ;
#802=( NAMED_UNIT ( * ) SI_UNIT ( $, .STERADIAN. ) SOLID_ANGLE_UNIT ( ) );
#803=DIRECTION ( 'NONE',  ( -1.000000000000000000, -0.000000000000000000, -0.000000000000000000 ) ) ;
#814=PLANE ( 'NONE',  #8086 ) ;
#819=UNCERTAINTY_MEASURE_WITH_UNIT (LENGTH_MEASURE( 1.000000000000000082E-05 ), #4668, 'distance_accuracy_value', 'NONE');
#824=CARTESIAN_POINT ( 'NONE',  ( 4.200000000000001954, 2.694222958124178486E-16, 2.200000000000001066 ) ) ;
#832=CARTESIAN_POINT ( 'NONE',  ( 4.200000000000001954, 0.000000000000000000, 2.000000000000000888 ) ) ;
#834=PRESENTATION_STYLE_ASSIGNMENT (( #959 ) ) ;
#849=LINE ( 'NONE', #5924, #7265 ) ;
#854=ORIENTED_EDGE ( 'NONE', *, *, #4472, .F. ) ;
#867=DIRECTION ( 'NONE',  ( 0.000000000000000000, -0.4999999999999990563, 0.8660254037844391517 ) ) ;
#868=( NAMED_UNIT ( * ) SI_UNIT ( $, .STERADIAN. ) SOLID_ANGLE_UNIT ( ) );
#874=DIRECTION ( 'NONE',  ( -1.000000000000000000, -0.000000000000000000, -0.000000000000000000 ) ) ;
#880=VECTOR ( 'NONE', #867, 1000.000000000000114 ) ;
#888=CARTESIAN_POINT ( 'NONE',  ( 2.000000000000000000, 0.8865213383406723713, 1.535499999999998755 ) ) ;
#893=ORIENTED_EDGE ( 'NONE', *, *, #4371, .F. ) ;
#906=PRODUCT_CONTEXT ( 'NONE', #2101, 'mechanical' ) ;
#915=AXIS2_PLACEMENT_3D ( 'NONE', #1550, #4798, #4708 ) ;
#918=SHAPE_REPRESENTATION_RELATIONSHIP ( 'NONE' , 'NONE' ,  #2201, #5769 ) ;
#937=DIRECTION ( 'NONE',  ( 0.000000000000000000, 0.000000000000000000, 1.000000000000000000 ) ) ;
#939=VERTEX_POINT ( 'NONE', #5198 ) ;
#952=CIRCLE ( 'NONE', #4810, 1.535500000000000087 ) ;
#959=SURFACE_STYLE_USAGE ( .BOTH. , #1639 ) ;
#973=VERTEX_POINT ( 'NONE', #1405 ) ;
#1003=CARTESIAN_POINT ( 'NONE',  ( 2.000000000000000000, 1.773042676681340968, -2.276824562219559311E-15 ) ) ;
#1035=AXIS2_PLACEMENT_3D ( 'NONE', #6976, #1250, #5657 ) ;
#1044=AXIS2_PLACEMENT_3D ( 'NONE', #5735, #7005, #1323 ) ;
#1050=ADVANCED_FACE ( 'NONE', ( #3273 ), #5771, .F. ) ;
#1060=COLOUR_RGB ( '', 0.40784314, 0.44705882, 0.49803922) ;
#1108=DIRECTION ( 'NONE',  ( 0.000000000000000000, 0.000000000000000000, -1.000000000000000000 ) ) ;
#1112=FACE_OUTER_BOUND ( 'NONE', #3633, .T. ) ;
#1114=FACE_BOUND ( 'NONE', #3753, .T. ) ;
#1133=ORIENTED_EDGE ( 'NONE', *, *, #5507, .T. ) ;
#1140=ORIENTED_EDGE ( 'NONE', *, *, #7176, .T. ) ;
#1142=CONICAL_SURFACE ( 'NONE', #3816, 1.610000000000000098, 0.7853981633974652654 ) ;
#1153=PLANE ( 'NONE',  #1035 ) ;
#1204=CARTESIAN_POINT ( 'NONE',  ( 20.00000000000000000, 1.610000000000000098, 0.000000000000000000 ) ) ;
#1206=DIRECTION ( 'NONE',  ( -0.000000000000000000, 0.000000000000000000, 1.000000000000000000 ) ) ;
#1215=DIRECTION ( 'NONE',  ( 0.000000000000000000, 0.4999999999999990008, -0.8660254037844391517 ) ) ;
#1216=VERTEX_POINT ( 'NONE', #2928 ) ;
#1225=CARTESIAN_POINT ( 'NONE',  ( 2.000000000000000000, -0.8865213383406685965, 1.535500000000000531 ) ) ;
#1246=CARTESIAN_POINT ( 'NONE',  ( 2.886521338340684917, 0.000000000000000000, 0.000000000000000000 ) ) ;
#1250=DIRECTION ( 'NONE',  ( 0.000000000000000000, -1.222984857324291014E-15, -1.000000000000000000 ) ) ;
#1257=EDGE_LOOP ( 'NONE', ( #5536, #2886 ) ) ;
#1261=DIRECTION ( 'NONE',  ( -1.000000000000000000, -0.000000000000000000, -0.000000000000000000 ) ) ;
#1289=DIRECTION ( 'NONE',  ( 0.000000000000000000, 0.000000000000000000, -1.000000000000000000 ) ) ;
#1291=CARTESIAN_POINT ( 'NONE',  ( 0.000000000000000000, 1.773042676681340968, -2.276824562219559311E-15 ) ) ;
#1292=TOROIDAL_SURFACE ( 'NONE', #2340, 3.299999999999999822, 0.2000000000000000111 ) ;
#1297=VERTEX_POINT ( 'NONE', #7663 ) ;
#1309=LINE ( 'NONE', #5835, #1866 ) ;
#1311=CARTESIAN_POINT ( 'NONE',  ( 2.000000000000000000, -0.8865213383406685965, 1.535500000000000531 ) ) ;
#1323=DIRECTION ( 'NONE',  ( 0.000000000000000000, 0.000000000000000000, 1.000000000000000000 ) ) ;
#1349=LINE ( 'NONE', #1971, #5962 ) ;
#1355=ORIENTED_EDGE ( 'NONE', *, *, #5972, .T. ) ;
#1387=EDGE_CURVE ( 'NONE', #3946, #4855, #388, .T. ) ;
#1388=CARTESIAN_POINT ( 'NONE',  ( 2.000000000000000000, 1.773042676681340968, -2.276824562219559311E-15 ) ) ;
#1405=CARTESIAN_POINT ( 'NONE',  ( 2.000000000000000000, 0.8865213383406723713, 1.535499999999998755 ) ) ;
#1413=ORIENTED_EDGE ( 'NONE', *, *, #5740, .T. ) ;
#1415=EDGE_LOOP ( 'NONE', ( #2634, #5708, #1140, #7987, #6582 ) ) ;
#1426=MANIFOLD_SOLID_BREP ( 'Hex', #644 ) ;
#1435=SURFACE_STYLE_FILL_AREA ( #5298 ) ;
#1438=DIRECTION ( 'NONE',  ( 0.000000000000000000, 0.000000000000000000, 1.000000000000000000 ) ) ;
#1453=AXIS2_PLACEMENT_3D ( 'NONE', #7511, #3899, #5229 ) ;
#1501=DIRECTION ( 'NONE',  ( 0.000000000000000000, 1.224646799147353207E-16, 1.000000000000000000 ) ) ;
#1504=ORIENTED_EDGE ( 'NONE', *, *, #6628, .F. ) ;
#1519=EDGE_CURVE ( 'NONE', #8200, #5522, #2299, .T. ) ;
#1524=ADVANCED_FACE ( 'NONE', ( #7492 ), #3504, .F. ) ;
#1542=EDGE_LOOP ( 'NONE', ( #8150, #4247, #311, #2237, #5971 ) ) ;
#1547=FILL_AREA_STYLE_COLOUR ( '', #2588 ) ;
#1550=CARTESIAN_POINT ( 'NONE',  ( 4.200000000000001954, 0.000000000000000000, -2.200000000000001066 ) ) ;
#1554=DIRECTION ( 'NONE',  ( -1.000000000000000000, -0.000000000000000000, -0.000000000000000000 ) ) ;
#1563=DIRECTION ( 'NONE',  ( 0.000000000000000000, 0.000000000000000000, 1.000000000000000000 ) ) ;
#1584=SHAPE_DEFINITION_REPRESENTATION ( #5, #2201 ) ;
#1587=AXIS2_PLACEMENT_3D ( 'NONE', #3942, #5152, #6454 ) ;
#1596=AXIS2_PLACEMENT_3D ( 'NONE', #4588, #6490, #3345 ) ;
#1599=ORIENTED_EDGE ( 'NONE', *, *, #5839, .F. ) ;
#1620=ORIENTED_EDGE ( 'NONE', *, *, #5507, .F. ) ;
#1623=LINE ( 'NONE', #8003, #4801 ) ;
#1639=SURFACE_SIDE_STYLE ('',( #6695 ) ) ;
#1651=DIRECTION ( 'NONE',  ( -1.000000000000000000, -0.000000000000000000, -0.000000000000000000 ) ) ;
#1664=CARTESIAN_POINT ( 'NONE',  ( 2.000000000000000000, 0.000000000000000000, 0.000000000000000000 ) ) ;
#1665=ADVANCED_FACE ( 'NONE', ( #2078 ), #1142, .T. ) ;
#1679=CARTESIAN_POINT ( 'NONE',  ( 2.000000000000000000, -0.8865213383406685965, 1.535500000000000531 ) ) ;
#1702=CARTESIAN_POINT ( 'NONE',  ( 2.000000000000000000, -1.773042676681340524, 1.734723475976807094E-15 ) ) ;
#1731=DIRECTION ( 'NONE',  ( 1.000000000000000000, 0.000000000000000000, 0.000000000000000000 ) ) ;
#1735=AXIS2_PLACEMENT_3D ( 'NONE', #4329, #1845, #3539 ) ;
#1766=EDGE_LOOP ( 'NONE', ( #6011, #2056, #6689, #6810, #2371 ) ) ;
#1783=CARTESIAN_POINT ( 'NONE',  ( 2.000000000000000000, 1.773042676681340968, -2.276824562219559311E-15 ) ) ;
#1791=LINE ( 'NONE', #4318, #6747 ) ;
#1797=ORIENTED_EDGE ( 'NONE', *, *, #4018, .F. ) ;
#1799=EDGE_LOOP ( 'NONE', ( #3663, #273, #7586, #8140, #3207 ) ) ;
#1845=DIRECTION ( 'NONE',  ( 1.000000000000000000, 0.000000000000000000, 0.000000000000000000 ) ) ;
#1852=CARTESIAN_POINT ( 'NONE',  ( 20.00000000000000355, 0.000000000000000000, 0.000000000000000000 ) ) ;
#1853=ORIENTED_EDGE ( 'NONE', *, *, #434, .T. ) ;
#1854=EDGE_CURVE ( 'NONE', #452, #2779, #609, .T. ) ;
#1866=VECTOR ( 'NONE', #6956, 1000.000000000000114 ) ;
#1868=EDGE_LOOP ( 'NONE', ( #6268, #1910, #893, #6773 ) ) ;
#1884=DIRECTION ( 'NONE',  ( 0.000000000000000000, -1.000000000000000000, 1.222984857324291014E-15 ) ) ;
#1886=ORIENTED_EDGE ( 'NONE', *, *, #1519, .T. ) ;
#1901=ADVANCED_FACE ( 'NONE', ( #7508 ), #2404, .F. ) ;
#1908=LINE ( 'NONE', #3776, #6937 ) ;
#1910=ORIENTED_EDGE ( 'NONE', *, *, #5481, .T. ) ;
#1914=CARTESIAN_POINT ( 'NONE',  ( 2.000000000000000000, -0.8865213383406685965, 1.535500000000000531 ) ) ;
#1925=FACE_OUTER_BOUND ( 'NONE', #6276, .T. ) ;
#1955=LINE ( 'NONE', #2535, #5535 ) ;
#1960=APPLICATION_CONTEXT ( 'automotive_design' ) ;
#1964=AXIS2_PLACEMENT_3D ( 'NONE', #3827, #6457, #2034 ) ;
#1965=ORIENTED_EDGE ( 'NONE', *, *, #6264, .F. ) ;
#1971=CARTESIAN_POINT ( 'NONE',  ( 0.000000000000000000, -0.8865213383406685965, 1.535500000000000531 ) ) ;
#1974=AXIS2_PLACEMENT_3D ( 'NONE', #7930, #6117, #5377 ) ;
#2005=CONICAL_SURFACE ( 'NONE', #7034, 1.610000000000000098, 0.7853981633974652654 ) ;
#2018=CARTESIAN_POINT ( 'NONE',  ( 0.000000000000000000, 0.8865213383406723713, 1.535499999999998755 ) ) ;
#2023=EDGE_CURVE ( 'NONE', #3366, #3705, #1955, .T. ) ;
#2031=CARTESIAN_POINT ( 'NONE',  ( 20.00000000000000355, 0.000000000000000000, 1.610000000000000098 ) ) ;
#2033=ADVANCED_FACE ( 'NONE', ( #7126 ), #7716, .T. ) ;
#2034=DIRECTION ( 'NONE',  ( 0.000000000000000000, 0.000000000000000000, 1.000000000000000000 ) ) ;
#2044=ORIENTED_EDGE ( 'NONE', *, *, #7176, .F. ) ;
#2056=ORIENTED_EDGE ( 'NONE', *, *, #8008, .F. ) ;
#2067=DIRECTION ( 'NONE',  ( 0.000000000000000000, -0.4999999999999990563, 0.8660254037844391517 ) ) ;
#2074=DIRECTION ( 'NONE',  ( -1.000000000000000000, -0.000000000000000000, -0.000000000000000000 ) ) ;
#2076=DIRECTION ( 'NONE',  ( 0.000000000000000000, -0.4999999999999990563, 0.8660254037844391517 ) ) ;
#2078=FACE_OUTER_BOUND ( 'NONE', #5602, .T. ) ;
#2080=ORIENTED_EDGE ( 'NONE', *, *, #6628, .T. ) ;
#2089=ORIENTED_EDGE ( 'NONE', *, *, #3355, .F. ) ;
#2098=DIRECTION ( 'NONE',  ( 0.000000000000000000, 0.000000000000000000, 1.000000000000000000 ) ) ;
#2101=APPLICATION_CONTEXT ( 'automotive_design' ) ;
#2119=EDGE_CURVE ( 'NONE', #4877, #5664, #952, .T. ) ;
#2147=LINE ( 'NONE', #3330, #2755 ) ;
#2160=CARTESIAN_POINT ( 'NONE',  ( 19.61000000000001720, 0.000000000000000000, 2.000000000000000888 ) ) ;
#2171=EDGE_CURVE ( 'NONE', #8104, #6902, #7460, .T. ) ;
#2182=EDGE_CURVE ( 'NONE', #4855, #2250, #5918, .T. ) ;
#2187=DIRECTION ( 'NONE',  ( 1.000000000000000000, 0.000000000000000000, 0.000000000000000000 ) ) ;
#2198=DIRECTION ( 'NONE',  ( 1.000000000000000000, 0.000000000000000000, 0.000000000000000000 ) ) ;
#2201=SHAPE_REPRESENTATION ( 'socket head cap screw_iso_ISO 4762 M4 x 16 - 16N', ( #1587 ), #3250 ) ;
#2202=VERTEX_POINT ( 'NONE', #2215 ) ;
#2215=CARTESIAN_POINT ( 'NONE',  ( 2.000000000000000000, -1.773042676681340524, 1.734723475976807094E-15 ) ) ;
#2222=CARTESIAN_POINT ( 'NONE',  ( 0.000000000000000000, 0.000000000000000000, 3.299999999999999822 ) ) ;
#2223=DIRECTION ( 'NONE',  ( 0.000000000000000000, 0.000000000000000000, 1.000000000000000000 ) ) ;
#2237=ORIENTED_EDGE ( 'NONE', *, *, #5989, .T. ) ;
#2238=CIRCLE ( 'NONE', #4505, 3.500000000000000000 ) ;
#2247=VECTOR ( 'NONE', #7078, 1000.000000000000114 ) ;
#2250=VERTEX_POINT ( 'NONE', #7500 ) ;
#2256=AXIS2_PLACEMENT_3D ( 'NONE', #6263, #4271, #7506 ) ;
#2264=CARTESIAN_POINT ( 'NONE',  ( 0.000000000000000000, -0.8865213383406685965, 1.535500000000000531 ) ) ;
#2283=PRODUCT_DEFINITION ( 'UNKNOWN', '', #4572, #2500 ) ;
#2292=ORIENTED_EDGE ( 'NONE', *, *, #434, .F. ) ;
#2299=LINE ( 'NONE', #6071, #2615 ) ;
#2300=EDGE_LOOP ( 'NONE', ( #4111, #3062, #1886, #6280 ) ) ;
#2310=DIRECTION ( 'NONE',  ( -1.000000000000000000, -0.000000000000000000, -0.000000000000000000 ) ) ;
#2313=CARTESIAN_POINT ( 'NONE',  ( 20.00000000000000355, 0.000000000000000000, 0.000000000000000000 ) ) ;
#2322=DIRECTION ( 'NONE',  ( 0.000000000000000000, 0.000000000000000000, -1.000000000000000000 ) ) ;
#2323=EDGE_CURVE ( 'NONE', #3305, #3366, #1908, .T. ) ;
#2340=AXIS2_PLACEMENT_3D ( 'NONE', #6042, #7904, #1563 ) ;
#2370=CIRCLE ( 'NONE', #646, 0.2000000000000000944 ) ;
#2371=ORIENTED_EDGE ( 'NONE', *, *, #4695, .T. ) ;
#2387=TOROIDAL_SURFACE ( 'NONE', #2783, 2.200000000000001066, 0.2000000000000000111 ) ;
#2404=PLANE ( 'NONE',  #206 ) ;
#2409=LINE ( 'NONE', #3694, #3437 ) ;
#2428=ORIENTED_EDGE ( 'NONE', *, *, #5839, .T. ) ;
#2472=DIRECTION ( 'NONE',  ( 0.000000000000000000, 0.000000000000000000, 1.000000000000000000 ) ) ;
#2478=VECTOR ( 'NONE', #1651, 1000.000000000000000 ) ;
#2500=PRODUCT_DEFINITION_CONTEXT ( 'detailed design', #1960, 'design' ) ;
#2506=DIRECTION ( 'NONE',  ( 0.000000000000000000, 0.000000000000000000, 1.000000000000000000 ) ) ;
#2511=DIRECTION ( 'NONE',  ( 0.000000000000000000, 0.000000000000000000, 1.000000000000000000 ) ) ;
#2522=DIRECTION ( 'NONE',  ( -1.000000000000000000, -0.000000000000000000, -0.000000000000000000 ) ) ;
#2535=CARTESIAN_POINT ( 'NONE',  ( 0.000000000000000000, 1.773042676681340968, -2.276824562219559311E-15 ) ) ;
#2546=CARTESIAN_POINT ( 'NONE',  ( 0.1999999999999987899, 0.000000000000000000, 0.000000000000000000 ) ) ;
#2555=CARTESIAN_POINT ( 'NONE',  ( 2.000000000000000000, 1.773042676681340968, -2.276824562219559311E-15 ) ) ;
#2557=CARTESIAN_POINT ( 'NONE',  ( 2.000000000000000000, 0.000000000000000000, 0.000000000000000000 ) ) ;
#2563=EDGE_CURVE ( 'NONE', #5522, #3297, #1623, .T. ) ;
#2573=DIRECTION ( 'NONE',  ( 1.000000000000000000, 0.000000000000000000, 0.000000000000000000 ) ) ;
#2574=LINE ( 'NONE', #4635, #3706 ) ;
#2587=EDGE_CURVE ( 'NONE', #1297, #5522, #4947, .T. ) ;
#2588=COLOUR_RGB ( '', 0.40784314, 0.44705882, 0.49803922) ;
#2594=ORIENTED_EDGE ( 'NONE', *, *, #2171, .F. ) ;
#2609=ORIENTED_EDGE ( 'NONE', *, *, #4925, .T. ) ;
#2613=CARTESIAN_POINT ( 'NONE',  ( 2.000000000000000000, 1.773042676681340968, -2.276824562219559311E-15 ) ) ;
#2615=VECTOR ( 'NONE', #331, 1000.000000000000114 ) ;
#2634=ORIENTED_EDGE ( 'NONE', *, *, #5972, .F. ) ;
#2644=AXIS2_PLACEMENT_3D ( 'NONE', #568, #3110, #3648 ) ;
#2680=SURFACE_STYLE_USAGE ( .BOTH. , #5259 ) ;
#2695=DIRECTION ( 'NONE',  ( 1.000000000000000000, 0.000000000000000000, 0.000000000000000000 ) ) ;
#2740=EDGE_CURVE ( 'NONE', #3297, #5311, #2808, .T. ) ;
#2755=VECTOR ( 'NONE', #3438, 1000.000000000000000 ) ;
#2778=AXIS2_PLACEMENT_3D ( 'NONE', #367, #413, #2955 ) ;
#2779=VERTEX_POINT ( 'NONE', #447 ) ;
#2783=AXIS2_PLACEMENT_3D ( 'NONE', #7248, #2187, #7336 ) ;
#2807=DIRECTION ( 'NONE',  ( 0.000000000000000000, 0.000000000000000000, 1.000000000000000000 ) ) ;
#2808=CIRCLE ( 'NONE', #277, 2.000000000000000888 ) ;
#2815=FACE_OUTER_BOUND ( 'NONE', #1868, .T. ) ;
#2838=CARTESIAN_POINT ( 'NONE',  ( 2.000000000000000000, -1.773042676681340524, 1.734723475976807094E-15 ) ) ;
#2873=( NAMED_UNIT ( * ) PLANE_ANGLE_UNIT ( ) SI_UNIT ( $, .RADIAN. ) );
#2886=ORIENTED_EDGE ( 'NONE', *, *, #8204, .T. ) ;
#2903=CIRCLE ( 'NONE', #1044, 1.610000000000000098 ) ;
#2906=FACE_OUTER_BOUND ( 'NONE', #1415, .T. ) ;
#2909=DIRECTION ( 'NONE',  ( 0.000000000000000000, 0.000000000000000000, 1.000000000000000000 ) ) ;
#2919=PLANE ( 'NONE',  #1974 ) ;
#2928=CARTESIAN_POINT ( 'NONE',  ( 2.000000000000000000, 0.8865213383406687075, -1.535500000000000975 ) ) ;
#2934=ORIENTED_EDGE ( 'NONE', *, *, #3030, .T. ) ;
#2948=AXIS2_PLACEMENT_3D ( 'NONE', #6681, #6104, #6767 ) ;
#2955=DIRECTION ( 'NONE',  ( 0.000000000000000000, 0.000000000000000000, 1.000000000000000000 ) ) ;
#3004=ADVANCED_FACE ( 'NONE', ( #3391 ), #1292, .T. ) ;
#3006=EDGE_CURVE ( 'NONE', #189, #2779, #5433, .T. ) ;
#3021=CARTESIAN_POINT ( 'NONE',  ( 2.000000000000000000, 1.773042676681340968, -2.276824562219559311E-15 ) ) ;
#3030=EDGE_CURVE ( 'NONE', #8200, #5903, #6989, .T. ) ;
#3041=AXIS2_PLACEMENT_3D ( 'NONE', #1003, #1731, #8113 ) ;
#3051=DIRECTION ( 'NONE',  ( 0.000000000000000000, 1.000000000000000000, -1.100686371591861952E-15 ) ) ;
#3062=ORIENTED_EDGE ( 'NONE', *, *, #4415, .T. ) ;
#3066=DIRECTION ( 'NONE',  ( -1.000000000000000000, -0.000000000000000000, -0.000000000000000000 ) ) ;
#3068=PLANE ( 'NONE',  #2256 ) ;
#3076=DIRECTION ( 'NONE',  ( 0.000000000000000000, 0.000000000000000000, -1.000000000000000000 ) ) ;
#3090=AXIS2_PLACEMENT_3D ( 'NONE', #5265, #1554, #6535 ) ;
#3102=EDGE_CURVE ( 'NONE', #5593, #6791, #6866, .T. ) ;
#3108=DIRECTION ( 'NONE',  ( 0.000000000000000000, 0.000000000000000000, 1.000000000000000000 ) ) ;
#3110=DIRECTION ( 'NONE',  ( -1.000000000000000000, -0.000000000000000000, -0.000000000000000000 ) ) ;
#3113=CARTESIAN_POINT ( 'NONE',  ( 0.000000000000000000, 0.8865213383406687075, -1.535500000000000975 ) ) ;
#3120=DIRECTION ( 'NONE',  ( 0.000000000000000000, 0.000000000000000000, 1.000000000000000000 ) ) ;
#3126=ORIENTED_EDGE ( 'NONE', *, *, #5156, .T. ) ;
#3143=( GEOMETRIC_REPRESENTATION_CONTEXT ( 3 ) GLOBAL_UNCERTAINTY_ASSIGNED_CONTEXT ( ( #4214 ) ) GLOBAL_UNIT_ASSIGNED_CONTEXT ( ( #3467, #5875, #802 ) ) REPRESENTATION_CONTEXT ( 'NONE', 'WORKASPACE' ) );
#3154=CARTESIAN_POINT ( 'NONE',  ( 2.000000000000000000, -1.329782007511006281, -0.7677499999999984892 ) ) ;
#3168=VERTEX_POINT ( 'NONE', #3814 ) ;
#3182=VERTEX_POINT ( 'NONE', #1311 ) ;
#3207=ORIENTED_EDGE ( 'NONE', *, *, #8008, .T. ) ;
#3243=DIRECTION ( 'NONE',  ( 0.000000000000000000, 0.000000000000000000, 1.000000000000000000 ) ) ;
#3250=( GEOMETRIC_REPRESENTATION_CONTEXT ( 3 ) GLOBAL_UNCERTAINTY_ASSIGNED_CONTEXT ( ( #3999 ) ) GLOBAL_UNIT_ASSIGNED_CONTEXT ( ( #7707, #140, #868 ) ) REPRESENTATION_CONTEXT ( 'NONE', 'WORKASPACE' ) );
#3257=DIRECTION ( 'NONE',  ( 0.000000000000000000, 1.000000000000000000, -1.100686371591861952E-15 ) ) ;
#3273=FACE_OUTER_BOUND ( 'NONE', #4969, .T. ) ;
#3278=CARTESIAN_POINT ( 'NONE',  ( -31.74999999999995737, 2.449293598294707893E-16, -2.000000000000000888 ) ) ;
#3297=VERTEX_POINT ( 'NONE', #832 ) ;
#3303=AXIS2_PLACEMENT_3D ( 'NONE', #4059, #2695, #186 ) ;
#3304=CIRCLE ( 'NONE', #501, 1.535500000000000087 ) ;
#3305=VERTEX_POINT ( 'NONE', #173 ) ;
#3309=CIRCLE ( 'NONE', #3571, 3.299999999999999822 ) ;
#3330=CARTESIAN_POINT ( 'NONE',  ( 2.000000000000000000, 0.000000000000000000, 1.535500000000000087 ) ) ;
#3345=DIRECTION ( 'NONE',  ( 0.000000000000000000, -1.224646799147353207E-16, 1.000000000000000000 ) ) ;
#3355=EDGE_CURVE ( 'NONE', #3305, #5664, #3968, .T. ) ;
#3366=VERTEX_POINT ( 'NONE', #5838 ) ;
#3369=LINE ( 'NONE', #3958, #4896 ) ;
#3373=ORIENTED_EDGE ( 'NONE', *, *, #4682, .F. ) ;
#3391=FACE_OUTER_BOUND ( 'NONE', #4293, .T. ) ;
#3409=ADVANCED_FACE ( 'NONE', ( #6694 ), #2919, .F. ) ;
#3435=CARTESIAN_POINT ( 'NONE',  ( 20.00000000000000355, 0.000000000000000000, 0.000000000000000000 ) ) ;
#3437=VECTOR ( 'NONE', #8133, 1000.000000000000227 ) ;
#3438=DIRECTION ( 'NONE',  ( -0.5000000000000061062, 0.000000000000000000, 0.8660254037844351549 ) ) ;
#3456=FACE_OUTER_BOUND ( 'NONE', #4185, .T. ) ;
#3467=( LENGTH_UNIT ( ) NAMED_UNIT ( * ) SI_UNIT ( .MILLI., .METRE. ) );
#3468=CARTESIAN_POINT ( 'NONE',  ( 0.000000000000000000, 0.000000000000000000, 0.000000000000000000 ) ) ;
#3478=CARTESIAN_POINT ( 'NONE',  ( 0.000000000000000000, 0.000000000000000000, 0.000000000000000000 ) ) ;
#3504=PLANE ( 'NONE',  #7518 ) ;
#3525=ORIENTED_EDGE ( 'NONE', *, *, #4636, .T. ) ;
#3530=CARTESIAN_POINT ( 'NONE',  ( -31.74999999999995737, 0.000000000000000000, 0.000000000000000000 ) ) ;
#3534=EDGE_LOOP ( 'NONE', ( #3126, #4868, #2044 ) ) ;
#3539=DIRECTION ( 'NONE',  ( 0.000000000000000000, 0.000000000000000000, -1.000000000000000000 ) ) ;
#3543=ORIENTED_EDGE ( 'NONE', *, *, #2323, .T. ) ;
#3571=AXIS2_PLACEMENT_3D ( 'NONE', #3468, #803, #2098 ) ;
#3591=ORIENTED_EDGE ( 'NONE', *, *, #2023, .T. ) ;
#3594=ORIENTED_EDGE ( 'NONE', *, *, #5740, .F. ) ;
#3631=ADVANCED_FACE ( 'NONE', ( #4964 ), #508, .F. ) ;
#3633=EDGE_LOOP ( 'NONE', ( #4436, #5010, #3926 ) ) ;
#3648=DIRECTION ( 'NONE',  ( 0.000000000000000000, 0.000000000000000000, -1.000000000000000000 ) ) ;
#3663=ORIENTED_EDGE ( 'NONE', *, *, #7763, .T. ) ;
#3691=ORIENTED_EDGE ( 'NONE', *, *, #665, .T. ) ;
#3694=CARTESIAN_POINT ( 'NONE',  ( 2.000000000000000000, -1.773042676681340524, 1.734723475976807094E-15 ) ) ;
#3695=CARTESIAN_POINT ( 'NONE',  ( 4.200000000000001954, 0.000000000000000000, 0.000000000000000000 ) ) ;
#3703=CIRCLE ( 'NONE', #7468, 2.000000000000000888 ) ;
#3705=VERTEX_POINT ( 'NONE', #2018 ) ;
#3706=VECTOR ( 'NONE', #727, 1000.000000000000000 ) ;
#3720=ADVANCED_FACE ( 'NONE', ( #7224 ), #5824, .T. ) ;
#3746=DIRECTION ( 'NONE',  ( 1.000000000000000000, 0.000000000000000000, 0.000000000000000000 ) ) ;
#3753=EDGE_LOOP ( 'NONE', ( #3591, #6487, #2609, #5360, #7242, #1797 ) ) ;
#3759=ORIENTED_EDGE ( 'NONE', *, *, #2587, .T. ) ;
#3774=CIRCLE ( 'NONE', #4773, 1.535500000000000087 ) ;
#3776=CARTESIAN_POINT ( 'NONE',  ( 2.000000000000000000, 1.773042676681340968, -2.276824562219559311E-15 ) ) ;
#3784=( GEOMETRIC_REPRESENTATION_CONTEXT ( 3 ) GLOBAL_UNCERTAINTY_ASSIGNED_CONTEXT ( ( #819 ) ) GLOBAL_UNIT_ASSIGNED_CONTEXT ( ( #4668, #2873, #6608 ) ) REPRESENTATION_CONTEXT ( 'NONE', 'WORKASPACE' ) );
#3804=ORIENTED_EDGE ( 'NONE', *, *, #5188, .F. ) ;
#3811=LINE ( 'NONE', #1225, #2247 ) ;
#3814=CARTESIAN_POINT ( 'NONE',  ( 2.000000000000000000, -1.877893248421449134E-15, -1.535500000000000087 ) ) ;
#3816=AXIS2_PLACEMENT_3D ( 'NONE', #1852, #4382, #2511 ) ;
#3827=CARTESIAN_POINT ( 'NONE',  ( -31.74999999999995737, 0.000000000000000000, 0.000000000000000000 ) ) ;
#3834=DIRECTION ( 'NONE',  ( 0.000000000000000000, -0.5000000000000011102, -0.8660254037844379305 ) ) ;
#3837=AXIS2_PLACEMENT_3D ( 'NONE', #3435, #2310, #2223 ) ;
#3871=CARTESIAN_POINT ( 'NONE',  ( 4.000000000000003553, 0.000000000000000000, 0.000000000000000000 ) ) ;
#3879=LINE ( 'NONE', #8177, #6752 ) ;
#3899=DIRECTION ( 'NONE',  ( -1.000000000000000000, -0.000000000000000000, -0.000000000000000000 ) ) ;
#3910=DIRECTION ( 'NONE',  ( 0.000000000000000000, -0.4999999999999990563, 0.8660254037844391517 ) ) ;
#3912=DIRECTION ( 'NONE',  ( -0.000000000000000000, 0.8660254037844391517, 0.4999999999999990563 ) ) ;
#3920=DIRECTION ( 'NONE',  ( 0.000000000000000000, 0.000000000000000000, -1.000000000000000000 ) ) ;
#3926=ORIENTED_EDGE ( 'NONE', *, *, #5689, .F. ) ;
#3927=ADVANCED_FACE ( 'NONE', ( #7262 ), #6592, .T. ) ;
#3941=MECHANICAL_DESIGN_GEOMETRIC_PRESENTATION_REPRESENTATION('',(#8099),#3143);
#3942=CARTESIAN_POINT ( 'NONE',  ( 0.000000000000000000, 0.000000000000000000, 0.000000000000000000 ) ) ;
#3946=VERTEX_POINT ( 'NONE', #449 ) ;
#3950=DIRECTION ( 'NONE',  ( -1.000000000000000000, -0.000000000000000000, -0.000000000000000000 ) ) ;
#3958=CARTESIAN_POINT ( 'NONE',  ( 2.000000000000000000, 1.773042676681340968, -2.276824562219559311E-15 ) ) ;
#3968=LINE ( 'NONE', #5908, #880 ) ;
#3969=TOROIDAL_SURFACE ( 'NONE', #5419, 3.299999999999999822, 0.2000000000000000111 ) ;
#3999=UNCERTAINTY_MEASURE_WITH_UNIT (LENGTH_MEASURE( 1.000000000000000082E-05 ), #7707, 'distance_accuracy_value', 'NONE');
#4016=ADVANCED_FACE ( 'NONE', ( #4283 ), #5620, .T. ) ;
#4018=EDGE_CURVE ( 'NONE', #3366, #452, #6977, .T. ) ;
#4019=DIRECTION ( 'NONE',  ( -1.000000000000000000, -0.000000000000000000, -0.000000000000000000 ) ) ;
#4026=CARTESIAN_POINT ( 'NONE',  ( 2.000000000000000000, 1.329782007511004727, -0.7677500000000019309 ) ) ;
#4029=DIRECTION ( 'NONE',  ( -1.000000000000000000, -0.000000000000000000, -0.000000000000000000 ) ) ;
#4036=EDGE_LOOP ( 'NONE', ( #3691, #1413, #854 ) ) ;
#4038=DIRECTION ( 'NONE',  ( 0.000000000000000000, -0.5000000000000011102, -0.8660254037844379305 ) ) ;
#4059=CARTESIAN_POINT ( 'NONE',  ( 0.1999999999999987899, 0.000000000000000000, 0.000000000000000000 ) ) ;
#4075=ADVANCED_FACE ( 'NONE', ( #4535 ), #814, .T. ) ;
#4111=ORIENTED_EDGE ( 'NONE', *, *, #6599, .F. ) ;
#4129=LINE ( 'NONE', #2838, #4511 ) ;
#4175=CARTESIAN_POINT ( 'NONE',  ( 2.000000000000000000, 0.000000000000000000, 0.000000000000000000 ) ) ;
#4176=ADVANCED_FACE ( 'NONE', ( #2815 ), #2387, .F. ) ;
#4185=EDGE_LOOP ( 'NONE', ( #6621, #7950, #4979 ) ) ;
#4192=DIRECTION ( 'NONE',  ( -1.000000000000000000, -0.000000000000000000, -0.000000000000000000 ) ) ;
#4212=ADVANCED_FACE ( 'NONE', ( #7993 ), #2005, .T. ) ;
#4214=UNCERTAINTY_MEASURE_WITH_UNIT (LENGTH_MEASURE( 1.000000000000000082E-05 ), #3467, 'distance_accuracy_value', 'NONE');
#4216=AXIS2_PLACEMENT_3D ( 'NONE', #3478, #6002, #2472 ) ;
#4226=AXIS2_PLACEMENT_3D ( 'NONE', #824, #4696, #1501 ) ;
#4247=ORIENTED_EDGE ( 'NONE', *, *, #2323, .F. ) ;
#4271=DIRECTION ( 'NONE',  ( 1.000000000000000000, 0.000000000000000000, 0.000000000000000000 ) ) ;
#4280=FACE_OUTER_BOUND ( 'NONE', #7887, .T. ) ;
#4283=FACE_OUTER_BOUND ( 'NONE', #5817, .T. ) ;
#4293=EDGE_LOOP ( 'NONE', ( #1965, #261, #5863, #6332 ) ) ;
#4318=CARTESIAN_POINT ( 'NONE',  ( 20.00000000000000355, 1.971681346627238735E-16, -1.610000000000000098 ) ) ;
#4322=ADVANCED_FACE ( 'NONE', ( #6882, #6796 ), #3068, .T. ) ;
#4326=ORIENTED_EDGE ( 'NONE', *, *, #4545, .F. ) ;
#4329=CARTESIAN_POINT ( 'NONE',  ( 4.200000000000001954, 0.000000000000000000, 0.000000000000000000 ) ) ;
#4355=DIRECTION ( 'NONE',  ( 1.000000000000000000, 0.000000000000000000, 0.000000000000000000 ) ) ;
#4371=EDGE_CURVE ( 'NONE', #7330, #939, #8074, .T. ) ;
#4382=DIRECTION ( 'NONE',  ( -1.000000000000000000, -0.000000000000000000, -0.000000000000000000 ) ) ;
#4415=EDGE_CURVE ( 'NONE', #5903, #8200, #2903, .T. ) ;
#4436=ORIENTED_EDGE ( 'NONE', *, *, #6594, .F. ) ;
#4448=PLANE ( 'NONE',  #5042 ) ;
#4451=DIRECTION ( 'NONE',  ( -1.000000000000000000, -0.000000000000000000, -0.000000000000000000 ) ) ;
#4472=EDGE_CURVE ( 'NONE', #554, #3168, #511, .T. ) ;
#4492=ORIENTED_EDGE ( 'NONE', *, *, #2119, .T. ) ;
#4505=AXIS2_PLACEMENT_3D ( 'NONE', #26, #2573, #5768 ) ;
#4509=ORIENTED_EDGE ( 'NONE', *, *, #4545, .T. ) ;
#4511=VECTOR ( 'NONE', #4019, 1000.000000000000000 ) ;
#4517=VECTOR ( 'NONE', #4830, 1000.000000000000000 ) ;
#4535=FACE_OUTER_BOUND ( 'NONE', #6009, .T. ) ;
#4545=EDGE_CURVE ( 'NONE', #2202, #8104, #2409, .T. ) ;
#4572=PRODUCT_DEFINITION_FORMATION_WITH_SPECIFIED_SOURCE ( 'ANY', '', #7499, .NOT_KNOWN. ) ;
#4588=CARTESIAN_POINT ( 'NONE',  ( 0.1999999999999987899, 4.041334437186265510E-16, -3.299999999999999822 ) ) ;
#4625=CIRCLE ( 'NONE', #3303, 3.500000000000000000 ) ;
#4635=CARTESIAN_POINT ( 'NONE',  ( 2.000000000000000000, 1.880445160090761061E-16, -1.535500000000000087 ) ) ;
#4636=EDGE_CURVE ( 'NONE', #6791, #5593, #3309, .T. ) ;
#4668=( LENGTH_UNIT ( ) NAMED_UNIT ( * ) SI_UNIT ( .MILLI., .METRE. ) );
#4682=EDGE_CURVE ( 'NONE', #5522, #1297, #6749, .T. ) ;
#4695=EDGE_CURVE ( 'NONE', #2202, #6632, #4129, .T. ) ;
#4696=DIRECTION ( 'NONE',  ( 0.000000000000000000, 1.000000000000000000, -1.224646799147353207E-16 ) ) ;
#4708=DIRECTION ( 'NONE',  ( 0.000000000000000000, 0.000000000000000000, -1.000000000000000000 ) ) ;
#4733=ADVANCED_FACE ( 'NONE', ( #8023 ), #7325, .F. ) ;
#4743=FILL_AREA_STYLE_COLOUR ( '', #1060 ) ;
#4746=VECTOR ( 'NONE', #1884, 1000.000000000000000 ) ;
#4773=AXIS2_PLACEMENT_3D ( 'NONE', #7894, #874, #7282 ) ;
#4797=LINE ( 'NONE', #1679, #118 ) ;
#4798=DIRECTION ( 'NONE',  ( 0.000000000000000000, -1.000000000000000000, 0.000000000000000000 ) ) ;
#4801=VECTOR ( 'NONE', #6722, 1000.000000000000000 ) ;
#4810=AXIS2_PLACEMENT_3D ( 'NONE', #4175, #7169, #2807 ) ;
#4830=DIRECTION ( 'NONE',  ( 0.000000000000000000, -1.000000000000000000, 1.222984857324291014E-15 ) ) ;
#4842=EDGE_CURVE ( 'NONE', #3182, #4877, #4797, .T. ) ;
#4855=VERTEX_POINT ( 'NONE', #87 ) ;
#4856=PLANE ( 'NONE',  #6219 ) ;
#4868=ORIENTED_EDGE ( 'NONE', *, *, #6337, .F. ) ;
#4877=VERTEX_POINT ( 'NONE', #6994 ) ;
#4886=AXIS2_PLACEMENT_3D ( 'NONE', #522, #566, #3108 ) ;
#4896=VECTOR ( 'NONE', #4038, 1000.000000000000114 ) ;
#4905=DIRECTION ( 'NONE',  ( 0.000000000000000000, 0.000000000000000000, 1.000000000000000000 ) ) ;
#4925=EDGE_CURVE ( 'NONE', #7076, #6632, #1309, .T. ) ;
#4947=CIRCLE ( 'NONE', #2948, 2.000000000000000888 ) ;
#4964=FACE_OUTER_BOUND ( 'NONE', #6904, .T. ) ;
#4969=EDGE_LOOP ( 'NONE', ( #4326, #352, #2594 ) ) ;
#4978=EDGE_CURVE ( 'NONE', #6902, #2202, #3811, .T. ) ;
#4979=ORIENTED_EDGE ( 'NONE', *, *, #2119, .F. ) ;
#4995=DIRECTION ( 'NONE',  ( 0.000000000000000000, 0.000000000000000000, 1.000000000000000000 ) ) ;
#5010=ORIENTED_EDGE ( 'NONE', *, *, #4842, .T. ) ;
#5042=AXIS2_PLACEMENT_3D ( 'NONE', #576, #6178, #1206 ) ;
#5047=ORIENTED_EDGE ( 'NONE', *, *, #1854, .T. ) ;
#5114=FACE_OUTER_BOUND ( 'NONE', #7268, .T. ) ;
#5122=VECTOR ( 'NONE', #107, 1000.000000000000000 ) ;
#5124=DIRECTION ( 'NONE',  ( 0.000000000000000000, 0.5000000000000009992, 0.8660254037844380415 ) ) ;
#5127=DIRECTION ( 'NONE',  ( -1.000000000000000000, -0.000000000000000000, -0.000000000000000000 ) ) ;
#5152=DIRECTION ( 'NONE',  ( 0.000000000000000000, 0.000000000000000000, 1.000000000000000000 ) ) ;
#5154=DIRECTION ( 'NONE',  ( 1.000000000000000000, 0.000000000000000000, 0.000000000000000000 ) ) ;
#5156=EDGE_CURVE ( 'NONE', #3168, #189, #6115, .T. ) ;
#5157=ORIENTED_EDGE ( 'NONE', *, *, #1387, .F. ) ;
#5158=DIRECTION ( 'NONE',  ( 0.000000000000000000, 0.8660254037844380415, -0.5000000000000009992 ) ) ;
#5176=AXIS2_PLACEMENT_3D ( 'NONE', #2557, #1261, #2506 ) ;
#5177=VECTOR ( 'NONE', #7915, 1000.000000000000227 ) ;
#5188=EDGE_CURVE ( 'NONE', #5664, #554, #6375, .T. ) ;
#5195=DIRECTION ( 'NONE',  ( -1.000000000000000000, -0.000000000000000000, -0.000000000000000000 ) ) ;
#5198=CARTESIAN_POINT ( 'NONE',  ( 4.000000000000001776, 2.694222958124178486E-16, 2.200000000000001066 ) ) ;
#5205=CARTESIAN_POINT ( 'NONE',  ( 2.000000000000000000, -0.8865213383406685965, 1.535500000000000531 ) ) ;
#5207=AXIS2_PLACEMENT_3D ( 'NONE', #2613, #5154, #7670 ) ;
#5213=DIRECTION ( 'NONE',  ( 0.000000000000000000, -0.5000000000000011102, -0.8660254037844379305 ) ) ;
#5229=DIRECTION ( 'NONE',  ( 0.000000000000000000, 0.000000000000000000, 1.000000000000000000 ) ) ;
#5249=DIRECTION ( 'NONE',  ( 0.000000000000000000, 0.000000000000000000, -1.000000000000000000 ) ) ;
#5259=SURFACE_SIDE_STYLE ('',( #1435 ) ) ;
#5265=CARTESIAN_POINT ( 'NONE',  ( 2.000000000000000000, 0.000000000000000000, 0.000000000000000000 ) ) ;
#5298=FILL_AREA_STYLE ('',( #4743 ) ) ;
#5311=VERTEX_POINT ( 'NONE', #546 ) ;
#5325=ORIENTED_EDGE ( 'NONE', *, *, #643, .F. ) ;
#5340=CARTESIAN_POINT ( 'NONE',  ( 4.000000000000003553, 0.000000000000000000, 0.000000000000000000 ) ) ;
#5341=ADVANCED_FACE ( 'NONE', ( #5788 ), #8180, .F. ) ;
#5360=ORIENTED_EDGE ( 'NONE', *, *, #643, .T. ) ;
#5377=DIRECTION ( 'NONE',  ( 0.000000000000000000, -1.000000000000000000, 1.100686371591861952E-15 ) ) ;
#5419=AXIS2_PLACEMENT_3D ( 'NONE', #2546, #5127, #3120 ) ;
#5433=LINE ( 'NONE', #7333, #2478 ) ;
#5481=EDGE_CURVE ( 'NONE', #3297, #939, #7266, .T. ) ;
#5485=EDGE_CURVE ( 'NONE', #7927, #6791, #2370, .T. ) ;
#5490=FACE_OUTER_BOUND ( 'NONE', #8021, .T. ) ;
#5504=DIRECTION ( 'NONE',  ( 0.000000000000000000, 0.8660254037844380415, -0.5000000000000012212 ) ) ;
#5506=AXIS2_PLACEMENT_3D ( 'NONE', #5205, #5158, #5124 ) ;
#5507=EDGE_CURVE ( 'NONE', #3305, #554, #3369, .T. ) ;
#5522=VERTEX_POINT ( 'NONE', #2160 ) ;
#5535=VECTOR ( 'NONE', #2067, 1000.000000000000114 ) ;
#5536=ORIENTED_EDGE ( 'NONE', *, *, #4371, .T. ) ;
#5541=ORIENTED_EDGE ( 'NONE', *, *, #6599, .T. ) ;
#5544=ORIENTED_EDGE ( 'NONE', *, *, #1519, .F. ) ;
#5557=CARTESIAN_POINT ( 'NONE',  ( 2.000000000000000000, -1.329782007511004727, 0.7677500000000014868 ) ) ;
#5559=LINE ( 'NONE', #1914, #114 ) ;
#5566=ADVANCED_FACE ( 'NONE', ( #3456 ), #5979, .F. ) ;
#5578=ORIENTED_EDGE ( 'NONE', *, *, #6337, .T. ) ;
#5587=FACE_OUTER_BOUND ( 'NONE', #7851, .T. ) ;
#5593=VERTEX_POINT ( 'NONE', #6142 ) ;
#5602=EDGE_LOOP ( 'NONE', ( #2934, #5541, #3373, #5544 ) ) ;
#5615=DIRECTION ( 'NONE',  ( 1.000000000000000000, 0.000000000000000000, 0.000000000000000000 ) ) ;
#5620=CYLINDRICAL_SURFACE ( 'NONE', #495, 3.500000000000000000 ) ;
#5632=ORIENTED_EDGE ( 'NONE', *, *, #4682, .T. ) ;
#5634=STYLED_ITEM ( 'NONE', ( #834 ), #5769 ) ;
#5657=DIRECTION ( 'NONE',  ( 0.000000000000000000, 1.000000000000000000, -1.222984857324291014E-15 ) ) ;
#5664=VERTEX_POINT ( 'NONE', #7968 ) ;
#5665=ORIENTED_EDGE ( 'NONE', *, *, #3006, .F. ) ;
#5678=CARTESIAN_POINT ( 'NONE',  ( 2.000000000000000000, -0.8865213383406685965, 1.535500000000000531 ) ) ;
#5689=EDGE_CURVE ( 'NONE', #6902, #4877, #3304, .T. ) ;
#5697=FACE_OUTER_BOUND ( 'NONE', #7840, .T. ) ;
#5701=EDGE_LOOP ( 'NONE', ( #7358, #7864, #5885, #389 ) ) ;
#5704=AXIS2_PLACEMENT_3D ( 'NONE', #5992, #209, #1438 ) ;
#5708=ORIENTED_EDGE ( 'NONE', *, *, #8123, .T. ) ;
#5715=VECTOR ( 'NONE', #7362, 1000.000000000000000 ) ;
#5735=CARTESIAN_POINT ( 'NONE',  ( 20.00000000000000355, 0.000000000000000000, 0.000000000000000000 ) ) ;
#5740=EDGE_CURVE ( 'NONE', #1216, #3168, #7479, .T. ) ;
#5766=ADVANCED_FACE ( 'NONE', ( #1925 ), #1153, .F. ) ;
#5768=DIRECTION ( 'NONE',  ( 0.000000000000000000, 0.000000000000000000, 1.000000000000000000 ) ) ;
#5769=ADVANCED_BREP_SHAPE_REPRESENTATION ( '', ( #1426, #1587 ), #3250 ) ;
#5771=PLANE ( 'NONE',  #5207 ) ;
#5788=FACE_OUTER_BOUND ( 'NONE', #8187, .T. ) ;
#5799=ADVANCED_FACE ( 'NONE', ( #5697 ), #3969, .T. ) ;
#5805=CARTESIAN_POINT ( 'NONE',  ( 4.000000000000000000, 0.000000000000000000, 0.000000000000000000 ) ) ;
#5809=FACE_OUTER_BOUND ( 'NONE', #1766, .T. ) ;
#5817=EDGE_LOOP ( 'NONE', ( #502, #1853, #6944, #2428 ) ) ;
#5824=PLANE ( 'NONE',  #368 ) ;
#5835=CARTESIAN_POINT ( 'NONE',  ( 0.000000000000000000, -0.8865213383406685965, 1.535500000000000531 ) ) ;
#5838=CARTESIAN_POINT ( 'NONE',  ( 0.000000000000000000, 1.773042676681340968, -2.276824562219559311E-15 ) ) ;
#5839=EDGE_CURVE ( 'NONE', #7927, #2250, #4625, .T. ) ;
#5849=TOROIDAL_SURFACE ( 'NONE', #1735, 2.200000000000001066, 0.2000000000000000111 ) ;
#5863=ORIENTED_EDGE ( 'NONE', *, *, #4636, .F. ) ;
#5868=ORIENTED_EDGE ( 'NONE', *, *, #665, .F. ) ;
#5875=( NAMED_UNIT ( * ) PLANE_ANGLE_UNIT ( ) SI_UNIT ( $, .RADIAN. ) );
#5878=EDGE_CURVE ( 'NONE', #3946, #7927, #7682, .T. ) ;
#5885=ORIENTED_EDGE ( 'NONE', *, *, #6264, .T. ) ;
#5890=CARTESIAN_POINT ( 'NONE',  ( 20.00000000000000355, 2.210487472460973191E-16, -1.610000000000000098 ) ) ;
#5897=ORIENTED_EDGE ( 'NONE', *, *, #7098, .T. ) ;
#5900=DIRECTION ( 'NONE',  ( 0.000000000000000000, 0.4999999999999991118, -0.8660254037844391517 ) ) ;
#5903=VERTEX_POINT ( 'NONE', #5890 ) ;
#5908=CARTESIAN_POINT ( 'NONE',  ( 2.000000000000000000, 1.773042676681340968, -2.276824562219559311E-15 ) ) ;
#5918=LINE ( 'NONE', #5996, #6658 ) ;
#5924=CARTESIAN_POINT ( 'NONE',  ( 2.000000000000000000, 0.8865213383406687075, -1.535500000000000975 ) ) ;
#5939=EDGE_CURVE ( 'NONE', #973, #3705, #7721, .T. ) ;
#5952=EDGE_CURVE ( 'NONE', #1216, #452, #849, .T. ) ;
#5962=VECTOR ( 'NONE', #3257, 1000.000000000000000 ) ;
#5965=CARTESIAN_POINT ( 'NONE',  ( 2.000000000000000000, 1.773042676681340968, -2.276824562219559311E-15 ) ) ;
#5971=ORIENTED_EDGE ( 'NONE', *, *, #5939, .T. ) ;
#5972=EDGE_CURVE ( 'NONE', #6551, #4877, #2147, .T. ) ;
#5977=LINE ( 'NONE', #1702, #5177 ) ;
#5979=PLANE ( 'NONE',  #6075 ) ;
#5989=EDGE_CURVE ( 'NONE', #5664, #973, #734, .T. ) ;
#5992=CARTESIAN_POINT ( 'NONE',  ( 19.61000000000001720, 0.000000000000000000, 0.000000000000000000 ) ) ;
#5996=CARTESIAN_POINT ( 'NONE',  ( -31.74999999999995737, 4.286263797015736595E-16, -3.500000000000000000 ) ) ;
#6002=DIRECTION ( 'NONE',  ( -1.000000000000000000, -0.000000000000000000, -0.000000000000000000 ) ) ;
#6009=EDGE_LOOP ( 'NONE', ( #5325, #507, #4509, #5578, #8048 ) ) ;
#6011=ORIENTED_EDGE ( 'NONE', *, *, #4925, .F. ) ;
#6017=DIRECTION ( 'NONE',  ( -1.000000000000000000, -0.000000000000000000, -0.000000000000000000 ) ) ;
#6042=CARTESIAN_POINT ( 'NONE',  ( 0.1999999999999987899, 0.000000000000000000, 0.000000000000000000 ) ) ;
#6071=CARTESIAN_POINT ( 'NONE',  ( 20.00000000000000355, 0.000000000000000000, 1.610000000000000098 ) ) ;
#6073=AXIS2_PLACEMENT_3D ( 'NONE', #3530, #6017, #2909 ) ;
#6075=AXIS2_PLACEMENT_3D ( 'NONE', #1388, #2198, #3920 ) ;
#6104=DIRECTION ( 'NONE',  ( -1.000000000000000000, -0.000000000000000000, -0.000000000000000000 ) ) ;
#6115=LINE ( 'NONE', #7487, #4517 ) ;
#6117=DIRECTION ( 'NONE',  ( -0.000000000000000000, 1.100686371591861952E-15, 1.000000000000000000 ) ) ;
#6142=CARTESIAN_POINT ( 'NONE',  ( 0.000000000000000000, 4.163799117101000559E-16, -3.299999999999999822 ) ) ;
#6143=ADVANCED_FACE ( 'NONE', ( #5114 ), #6261, .T. ) ;
#6145=ORIENTED_EDGE ( 'NONE', *, *, #5952, .T. ) ;
#6178=DIRECTION ( 'NONE',  ( -1.000000000000000000, 0.000000000000000000, -0.000000000000000000 ) ) ;
#6184=ORIENTED_EDGE ( 'NONE', *, *, #4415, .F. ) ;
#6207=AXIS2_PLACEMENT_3D ( 'NONE', #2555, #676, #6322 ) ;
#6209=ORIENTED_EDGE ( 'NONE', *, *, #5481, .F. ) ;
#6219=AXIS2_PLACEMENT_3D ( 'NONE', #1204, #3746, #2322 ) ;
#6224=DIRECTION ( 'NONE',  ( 0.000000000000000000, 0.000000000000000000, -1.000000000000000000 ) ) ;
#6230=CARTESIAN_POINT ( 'NONE',  ( -31.74999999999995737, 0.000000000000000000, 0.000000000000000000 ) ) ;
#6261=CYLINDRICAL_SURFACE ( 'NONE', #4886, 2.000000000000000888 ) ;
#6263=CARTESIAN_POINT ( 'NONE',  ( 4.000000000000000000, 3.500000000000000000, 0.000000000000000000 ) ) ;
#6264=EDGE_CURVE ( 'NONE', #2250, #7927, #2238, .T. ) ;
#6268=ORIENTED_EDGE ( 'NONE', *, *, #2740, .F. ) ;
#6276=EDGE_LOOP ( 'NONE', ( #5047, #5665, #6923, #3594, #6145 ) ) ;
#6280=ORIENTED_EDGE ( 'NONE', *, *, #2587, .F. ) ;
#6292=LINE ( 'NONE', #5678, #5715 ) ;
#6319=ADVANCED_FACE ( 'NONE', ( #2906 ), #8065, .F. ) ;
#6322=DIRECTION ( 'NONE',  ( 0.000000000000000000, 0.000000000000000000, -1.000000000000000000 ) ) ;
#6332=ORIENTED_EDGE ( 'NONE', *, *, #5485, .F. ) ;
#6337=EDGE_CURVE ( 'NONE', #8104, #189, #5977, .T. ) ;
#6375=CIRCLE ( 'NONE', #2778, 1.535500000000000087 ) ;
#6397=DIRECTION ( 'NONE',  ( -1.000000000000000000, -0.000000000000000000, -0.000000000000000000 ) ) ;
#6398=CARTESIAN_POINT ( 'NONE',  ( 2.000000000000000000, 0.8865213383406687075, -1.535500000000000975 ) ) ;
#6411=CARTESIAN_POINT ( 'NONE',  ( 2.000000000000000000, 1.773042676681340968, -2.276824562219559311E-15 ) ) ;
#6429=AXIS2_PLACEMENT_3D ( 'NONE', #3871, #6397, #3243 ) ;
#6431=PLANE ( 'NONE',  #5506 ) ;
#6454=DIRECTION ( 'NONE',  ( 1.000000000000000000, 0.000000000000000000, 0.000000000000000000 ) ) ;
#6457=DIRECTION ( 'NONE',  ( -1.000000000000000000, -0.000000000000000000, -0.000000000000000000 ) ) ;
#6470=VECTOR ( 'NONE', #4029, 1000.000000000000000 ) ;
#6487=ORIENTED_EDGE ( 'NONE', *, *, #7763, .F. ) ;
#6490=DIRECTION ( 'NONE',  ( -0.000000000000000000, 1.000000000000000000, 1.224646799147353207E-16 ) ) ;
#6506=CARTESIAN_POINT ( 'NONE',  ( 0.000000000000000000, 0.8865213383406687075, -1.535500000000000975 ) ) ;
#6528=DIRECTION ( 'NONE',  ( -1.000000000000000000, -0.000000000000000000, -0.000000000000000000 ) ) ;
#6535=DIRECTION ( 'NONE',  ( 0.000000000000000000, 0.000000000000000000, 1.000000000000000000 ) ) ;
#6537=ADVANCED_FACE ( 'NONE', ( #1114, #4280 ), #4448, .T. ) ;
#6551=VERTEX_POINT ( 'NONE', #1246 ) ;
#6563=PRESENTATION_STYLE_ASSIGNMENT (( #2680 ) ) ;
#6573=ORIENTED_EDGE ( 'NONE', *, *, #8123, .F. ) ;
#6582=ORIENTED_EDGE ( 'NONE', *, *, #5689, .T. ) ;
#6592=CYLINDRICAL_SURFACE ( 'NONE', #6073, 3.500000000000000000 ) ;
#6594=EDGE_CURVE ( 'NONE', #3182, #6902, #7476, .T. ) ;
#6599=EDGE_CURVE ( 'NONE', #5903, #1297, #1791, .T. ) ;
#6608=( NAMED_UNIT ( * ) SI_UNIT ( $, .STERADIAN. ) SOLID_ANGLE_UNIT ( ) );
#6621=ORIENTED_EDGE ( 'NONE', *, *, #7207, .T. ) ;
#6628=EDGE_CURVE ( 'NONE', #5311, #3297, #3703, .T. ) ;
#6629=DIRECTION ( 'NONE',  ( -1.000000000000000000, -0.000000000000000000, -0.000000000000000000 ) ) ;
#6632=VERTEX_POINT ( 'NONE', #184 ) ;
#6652=FILL_AREA_STYLE ('',( #1547 ) ) ;
#6658=VECTOR ( 'NONE', #212, 1000.000000000000000 ) ;
#6681=CARTESIAN_POINT ( 'NONE',  ( 19.61000000000001720, 0.000000000000000000, 0.000000000000000000 ) ) ;
#6689=ORIENTED_EDGE ( 'NONE', *, *, #6594, .T. ) ;
#6691=CIRCLE ( 'NONE', #6429, 3.500000000000000000 ) ;
#6694=FACE_OUTER_BOUND ( 'NONE', #1799, .T. ) ;
#6695=SURFACE_STYLE_FILL_AREA ( #6652 ) ;
#6714=ORIENTED_EDGE ( 'NONE', *, *, #2563, .F. ) ;
#6717=VECTOR ( 'NONE', #571, 1000.000000000000000 ) ;
#6722=DIRECTION ( 'NONE',  ( -1.000000000000000000, -0.000000000000000000, -0.000000000000000000 ) ) ;
#6723=DIRECTION ( 'NONE',  ( 0.000000000000000000, 0.000000000000000000, 1.000000000000000000 ) ) ;
#6747=VECTOR ( 'NONE', #6845, 1000.000000000000114 ) ;
#6749=CIRCLE ( 'NONE', #5704, 2.000000000000000888 ) ;
#6752=VECTOR ( 'NONE', #1215, 1000.000000000000227 ) ;
#6757=CIRCLE ( 'NONE', #1596, 0.2000000000000000944 ) ;
#6767=DIRECTION ( 'NONE',  ( 0.000000000000000000, 0.000000000000000000, 1.000000000000000000 ) ) ;
#6773=ORIENTED_EDGE ( 'NONE', *, *, #7098, .F. ) ;
#6783=EDGE_LOOP ( 'NONE', ( #5157, #2292 ) ) ;
#6791=VERTEX_POINT ( 'NONE', #2222 ) ;
#6796=FACE_OUTER_BOUND ( 'NONE', #6783, .T. ) ;
#6805=DIRECTION ( 'NONE',  ( 0.000000000000000000, -0.5000000000000009992, -0.8660254037844380415 ) ) ;
#6810=ORIENTED_EDGE ( 'NONE', *, *, #4978, .T. ) ;
#6845=DIRECTION ( 'NONE',  ( -0.7071067811865355823, 8.659560562355079537E-17, -0.7071067811865595631 ) ) ;
#6846=CARTESIAN_POINT ( 'NONE',  ( 4.200000000000001954, 0.000000000000000000, 0.000000000000000000 ) ) ;
#6866=CIRCLE ( 'NONE', #4216, 3.299999999999999822 ) ;
#6882=FACE_BOUND ( 'NONE', #1257, .T. ) ;
#6902=VERTEX_POINT ( 'NONE', #5557 ) ;
#6904=EDGE_LOOP ( 'NONE', ( #6573, #1355, #4492, #214, #6991 ) ) ;
#6914=ORIENTED_EDGE ( 'NONE', *, *, #3102, .T. ) ;
#6923=ORIENTED_EDGE ( 'NONE', *, *, #5156, .F. ) ;
#6937=VECTOR ( 'NONE', #2522, 1000.000000000000000 ) ;
#6944=ORIENTED_EDGE ( 'NONE', *, *, #5878, .T. ) ;
#6956=DIRECTION ( 'NONE',  ( 0.000000000000000000, -0.5000000000000009992, -0.8660254037844380415 ) ) ;
#6974=DIRECTION ( 'NONE',  ( 1.000000000000000000, 0.000000000000000000, 0.000000000000000000 ) ) ;
#6976=CARTESIAN_POINT ( 'NONE',  ( 2.000000000000000000, 0.8865213383406687075, -1.535500000000000975 ) ) ;
#6977=LINE ( 'NONE', #1291, #7921 ) ;
#6989=CIRCLE ( 'NONE', #3837, 1.610000000000000098 ) ;
#6991=ORIENTED_EDGE ( 'NONE', *, *, #4472, .T. ) ;
#6994=CARTESIAN_POINT ( 'NONE',  ( 2.000000000000000000, 1.690103923579303787E-15, 1.535499999999999865 ) ) ;
#7005=DIRECTION ( 'NONE',  ( -1.000000000000000000, -0.000000000000000000, -0.000000000000000000 ) ) ;
#7034=AXIS2_PLACEMENT_3D ( 'NONE', #2313, #6629, #937 ) ;
#7076=VERTEX_POINT ( 'NONE', #2264 ) ;
#7078=DIRECTION ( 'NONE',  ( 0.000000000000000000, -0.5000000000000009992, -0.8660254037844380415 ) ) ;
#7097=CARTESIAN_POINT ( 'NONE',  ( -31.74999999999995737, 0.000000000000000000, 3.500000000000000000 ) ) ;
#7098=EDGE_CURVE ( 'NONE', #5311, #7330, #378, .T. ) ;
#7126=FACE_OUTER_BOUND ( 'NONE', #668, .T. ) ;
#7148=CIRCLE ( 'NONE', #7280, 2.200000000000001066 ) ;
#7169=DIRECTION ( 'NONE',  ( -1.000000000000000000, -0.000000000000000000, -0.000000000000000000 ) ) ;
#7176=EDGE_CURVE ( 'NONE', #3168, #8104, #3774, .T. ) ;
#7207=EDGE_CURVE ( 'NONE', #4877, #973, #6292, .T. ) ;
#7224=FACE_OUTER_BOUND ( 'NONE', #1542, .T. ) ;
#7242=ORIENTED_EDGE ( 'NONE', *, *, #1854, .F. ) ;
#7248=CARTESIAN_POINT ( 'NONE',  ( 4.200000000000001954, 0.000000000000000000, 0.000000000000000000 ) ) ;
#7262=FACE_OUTER_BOUND ( 'NONE', #5701, .T. ) ;
#7265=VECTOR ( 'NONE', #3950, 1000.000000000000000 ) ;
#7266=CIRCLE ( 'NONE', #4226, 0.2000000000000000944 ) ;
#7268=EDGE_LOOP ( 'NONE', ( #5632, #283, #2080, #6714 ) ) ;
#7274=VECTOR ( 'NONE', #6805, 1000.000000000000114 ) ;
#7280=AXIS2_PLACEMENT_3D ( 'NONE', #5805, #5195, #7714 ) ;
#7282=DIRECTION ( 'NONE',  ( 0.000000000000000000, 0.000000000000000000, 1.000000000000000000 ) ) ;
#7325=PLANE ( 'NONE',  #3041 ) ;
#7330=VERTEX_POINT ( 'NONE', #7742 ) ;
#7333=CARTESIAN_POINT ( 'NONE',  ( 2.000000000000000000, -0.8865213383406721492, -1.535499999999998977 ) ) ;
#7336=DIRECTION ( 'NONE',  ( 0.000000000000000000, 0.000000000000000000, -1.000000000000000000 ) ) ;
#7341=EDGE_CURVE ( 'NONE', #2250, #5593, #6757, .T. ) ;
#7358=ORIENTED_EDGE ( 'NONE', *, *, #1387, .T. ) ;
#7362=DIRECTION ( 'NONE',  ( 0.000000000000000000, 1.000000000000000000, -1.100686371591861952E-15 ) ) ;
#7378=DIRECTION ( 'NONE',  ( 1.000000000000000000, 0.000000000000000000, 0.000000000000000000 ) ) ;
#7432=CARTESIAN_POINT ( 'NONE',  ( 2.000000000000000000, -0.8865213383406685965, 1.535500000000000531 ) ) ;
#7460=CIRCLE ( 'NONE', #3090, 1.535500000000000087 ) ;
#7468=AXIS2_PLACEMENT_3D ( 'NONE', #3695, #5615, #3076 ) ;
#7476=LINE ( 'NONE', #7432, #7274 ) ;
#7479=LINE ( 'NONE', #6398, #4746 ) ;
#7487=CARTESIAN_POINT ( 'NONE',  ( 2.000000000000000000, 0.8865213383406687075, -1.535500000000000975 ) ) ;
#7492=FACE_OUTER_BOUND ( 'NONE', #170, .T. ) ;
#7499=PRODUCT ( 'socket head cap screw_iso_ISO 4762 M4 x 16 - 16N', 'socket head cap screw_iso_ISO 4762 M4 x 16 - 16N', '', ( #906 ) ) ;
#7500=CARTESIAN_POINT ( 'NONE',  ( 0.1999999999999987899, 4.286263797015736595E-16, -3.500000000000000000 ) ) ;
#7506=DIRECTION ( 'NONE',  ( 0.000000000000000000, 0.000000000000000000, -1.000000000000000000 ) ) ;
#7508=FACE_OUTER_BOUND ( 'NONE', #4036, .T. ) ;
#7511=CARTESIAN_POINT ( 'NONE',  ( 2.000000000000000000, 0.000000000000000000, 0.000000000000000000 ) ) ;
#7518=AXIS2_PLACEMENT_3D ( 'NONE', #8060, #5504, #462 ) ;
#7572=CARTESIAN_POINT ( 'NONE',  ( 2.000000000000000000, 1.773042676681340968, -2.276824562219559311E-15 ) ) ;
#7586=ORIENTED_EDGE ( 'NONE', *, *, #7207, .F. ) ;
#7611=ADVANCED_FACE ( 'NONE', ( #5587 ), #5849, .F. ) ;
#7663=CARTESIAN_POINT ( 'NONE',  ( 19.61000000000001720, 2.449293598294707893E-16, -2.000000000000000888 ) ) ;
#7670=DIRECTION ( 'NONE',  ( 0.000000000000000000, 0.000000000000000000, -1.000000000000000000 ) ) ;
#7682=LINE ( 'NONE', #7097, #8058 ) ;
#7684=AXIS2_PLACEMENT_3D ( 'NONE', #3021, #4355, #6224 ) ;
#7694=VECTOR ( 'NONE', #5213, 1000.000000000000114 ) ;
#7707=( LENGTH_UNIT ( ) NAMED_UNIT ( * ) SI_UNIT ( .MILLI., .METRE. ) );
#7708=AXIS2_PLACEMENT_3D ( 'NONE', #5340, #6528, #208 ) ;
#7714=DIRECTION ( 'NONE',  ( 0.000000000000000000, 0.000000000000000000, -1.000000000000000000 ) ) ;
#7716=CYLINDRICAL_SURFACE ( 'NONE', #1964, 2.000000000000000888 ) ;
#7721=LINE ( 'NONE', #888, #6470 ) ;
#7722=CARTESIAN_POINT ( 'NONE',  ( 2.000000000000000000, -1.773042676681340524, 1.734723475976807094E-15 ) ) ;
#7732=CARTESIAN_POINT ( 'NONE',  ( 0.1999999999999987899, 0.000000000000000000, 3.299999999999999822 ) ) ;
#7742=CARTESIAN_POINT ( 'NONE',  ( 4.000000000000001776, 0.000000000000000000, -2.200000000000001066 ) ) ;
#7758=ORIENTED_EDGE ( 'NONE', *, *, #3030, .F. ) ;
#7763=EDGE_CURVE ( 'NONE', #7076, #3705, #1349, .T. ) ;
#7765=DIRECTION ( 'NONE',  ( 0.000000000000000000, -0.8660254037844391517, -0.4999999999999991118 ) ) ;
#7798=VECTOR ( 'NONE', #3910, 1000.000000000000114 ) ;
#7840=EDGE_LOOP ( 'NONE', ( #7960, #1599, #7909, #7934 ) ) ;
#7851=EDGE_LOOP ( 'NONE', ( #6209, #1504, #5897, #199 ) ) ;
#7864=ORIENTED_EDGE ( 'NONE', *, *, #2182, .T. ) ;
#7880=DIRECTION ( 'NONE',  ( -1.000000000000000000, -0.000000000000000000, -0.000000000000000000 ) ) ;
#7883=DIRECTION ( 'NONE',  ( 0.000000000000000000, -1.000000000000000000, 0.000000000000000000 ) ) ;
#7887=EDGE_LOOP ( 'NONE', ( #3525, #6914 ) ) ;
#7894=CARTESIAN_POINT ( 'NONE',  ( 2.000000000000000000, 0.000000000000000000, 0.000000000000000000 ) ) ;
#7904=DIRECTION ( 'NONE',  ( -1.000000000000000000, -0.000000000000000000, -0.000000000000000000 ) ) ;
#7906=CARTESIAN_POINT ( 'NONE',  ( 0.1999999999999987899, 0.000000000000000000, 3.500000000000000000 ) ) ;
#7909=ORIENTED_EDGE ( 'NONE', *, *, #5485, .T. ) ;
#7915=DIRECTION ( 'NONE',  ( 0.000000000000000000, 0.4999999999999990008, -0.8660254037844391517 ) ) ;
#7921=VECTOR ( 'NONE', #3834, 1000.000000000000114 ) ;
#7927=VERTEX_POINT ( 'NONE', #7906 ) ;
#7930=CARTESIAN_POINT ( 'NONE',  ( 2.000000000000000000, -0.8865213383406685965, 1.535500000000000531 ) ) ;
#7931=AXIS2_PLACEMENT_3D ( 'NONE', #7965, #7880, #4905 ) ;
#7934=ORIENTED_EDGE ( 'NONE', *, *, #3102, .F. ) ;
#7950=ORIENTED_EDGE ( 'NONE', *, *, #5989, .F. ) ;
#7960=ORIENTED_EDGE ( 'NONE', *, *, #7341, .F. ) ;
#7964=PLANE ( 'NONE',  #7684 ) ;
#7965=CARTESIAN_POINT ( 'NONE',  ( 2.000000000000000000, 0.000000000000000000, 0.000000000000000000 ) ) ;
#7968=CARTESIAN_POINT ( 'NONE',  ( 2.000000000000000000, 1.329782007511006725, 0.7677499999999987113 ) ) ;
#7987=ORIENTED_EDGE ( 'NONE', *, *, #2171, .T. ) ;
#7988=ORIENTED_EDGE ( 'NONE', *, *, #342, .F. ) ;
#7993=FACE_OUTER_BOUND ( 'NONE', #2300, .T. ) ;
#8003=CARTESIAN_POINT ( 'NONE',  ( -31.74999999999995737, 0.000000000000000000, 2.000000000000000888 ) ) ;
#8008=EDGE_CURVE ( 'NONE', #3182, #7076, #5559, .T. ) ;
#8021=EDGE_LOOP ( 'NONE', ( #7758, #6184 ) ) ;
#8023=FACE_OUTER_BOUND ( 'NONE', #3534, .T. ) ;
#8048=ORIENTED_EDGE ( 'NONE', *, *, #3006, .T. ) ;
#8058=VECTOR ( 'NONE', #2074, 1000.000000000000000 ) ;
#8060=CARTESIAN_POINT ( 'NONE',  ( 2.000000000000000000, 1.773042676681340968, -2.276824562219559311E-15 ) ) ;
#8065=CONICAL_SURFACE ( 'NONE', #7931, 1.535500000000000087, 1.047197551196590748 ) ;
#8074=CIRCLE ( 'NONE', #2644, 2.200000000000001066 ) ;
#8086=AXIS2_PLACEMENT_3D ( 'NONE', #7722, #3912, #2076 ) ;
#8093=CARTESIAN_POINT ( 'NONE',  ( 2.000000000000000000, -0.8865213383406721492, -1.535499999999998977 ) ) ;
#8099=STYLED_ITEM ( 'NONE', ( #6563 ), #1426 ) ;
#8104=VERTEX_POINT ( 'NONE', #3154 ) ;
#8113=DIRECTION ( 'NONE',  ( 0.000000000000000000, 0.000000000000000000, -1.000000000000000000 ) ) ;
#8123=EDGE_CURVE ( 'NONE', #6551, #3168, #2574, .T. ) ;
#8133=DIRECTION ( 'NONE',  ( 0.000000000000000000, 0.4999999999999990008, -0.8660254037844391517 ) ) ;
#8140=ORIENTED_EDGE ( 'NONE', *, *, #4842, .F. ) ;
#8150=ORIENTED_EDGE ( 'NONE', *, *, #2023, .F. ) ;
#8177=CARTESIAN_POINT ( 'NONE',  ( 0.000000000000000000, -1.773042676681340524, 1.734723475976807094E-15 ) ) ;
#8180=PLANE ( 'NONE',  #6207 ) ;
#8187=EDGE_LOOP ( 'NONE', ( #2089, #1133, #3804 ) ) ;
#8200=VERTEX_POINT ( 'NONE', #2031 ) ;
#8204=EDGE_CURVE ( 'NONE', #939, #7330, #7148, .T. ) ;
ENDSEC;
END-ISO-10303-21;
